ISO-10303-21;
HEADER;
/* Generated by software containing ST-Developer
 * from STEP Tools, Inc. (www.steptools.com) 
 */

FILE_DESCRIPTION(
/* description */ ('Bearing-mounted hook block'),
/* implementation_level */ '2;1');

FILE_NAME(
/* name */ 'M16 hook retaining nut.step',
/* time_stamp */ '2026-10-28T22:30:11-07:00',
/* author */ (''),
/* organization */ (''),
/* preprocessor_version */ 'ST-DEVELOPER v20.2',
/* originating_system */ 'Autodesk Translation Framework v15.17.0.0',
/* authorisation */ '');

FILE_SCHEMA (('AUTOMOTIVE_DESIGN { 1 0 10303 214 3 1 1 }'));
ENDSEC;

DATA;
#10=MECHANICAL_DESIGN_GEOMETRIC_PRESENTATION_REPRESENTATION('',(#354),#7609);
#298=SHAPE_REPRESENTATION_RELATIONSHIP('SRR','None',#7748,#322);
#322=ADVANCED_BREP_SHAPE_REPRESENTATION('',(#383),#7608);
#354=STYLED_ITEM('',(#7938),#383);
#383=MANIFOLD_SOLID_BREP('Body1',#3953);
#595=LINE('',#7504,#825);
#596=LINE('',#7509,#826);
#597=LINE('',#7511,#827);
#598=LINE('',#7513,#828);
#599=LINE('',#7514,#829);
#600=LINE('',#7517,#830);
#601=LINE('',#7519,#831);
#602=LINE('',#7520,#832);
#603=LINE('',#7523,#833);
#604=LINE('',#7525,#834);
#605=LINE('',#7526,#835);
#606=LINE('',#7529,#836);
#607=LINE('',#7531,#837);
#608=LINE('',#7532,#838);
#609=LINE('',#7535,#839);
#610=LINE('',#7537,#840);
#611=LINE('',#7538,#841);
#612=LINE('',#7540,#842);
#613=LINE('',#7541,#843);
#825=VECTOR('',#6014,0.7);
#826=VECTOR('',#6019,1.);
#827=VECTOR('',#6020,1.);
#828=VECTOR('',#6021,1.);
#829=VECTOR('',#6022,1.);
#830=VECTOR('',#6025,1.);
#831=VECTOR('',#6026,1.);
#832=VECTOR('',#6027,1.);
#833=VECTOR('',#6030,1.);
#834=VECTOR('',#6031,1.);
#835=VECTOR('',#6032,1.);
#836=VECTOR('',#6035,1.);
#837=VECTOR('',#6036,1.);
#838=VECTOR('',#6037,1.);
#839=VECTOR('',#6040,1.);
#840=VECTOR('',#6041,1.);
#841=VECTOR('',#6042,1.);
#842=VECTOR('',#6045,1.);
#843=VECTOR('',#6046,1.);
#920=CYLINDRICAL_SURFACE('',#4740,0.7);
#999=FACE_BOUND('',#1550,.T.);
#1000=FACE_BOUND('',#1552,.T.);
#1228=FACE_OUTER_BOUND('',#1542,.T.);
#1229=FACE_OUTER_BOUND('',#1543,.T.);
#1230=FACE_OUTER_BOUND('',#1544,.T.);
#1231=FACE_OUTER_BOUND('',#1545,.T.);
#1232=FACE_OUTER_BOUND('',#1546,.T.);
#1233=FACE_OUTER_BOUND('',#1547,.T.);
#1234=FACE_OUTER_BOUND('',#1548,.T.);
#1235=FACE_OUTER_BOUND('',#1549,.T.);
#1236=FACE_OUTER_BOUND('',#1551,.T.);
#1542=EDGE_LOOP('',(#3518,#3519,#3520,#3521));
#1543=EDGE_LOOP('',(#3522,#3523,#3524,#3525));
#1544=EDGE_LOOP('',(#3526,#3527,#3528,#3529));
#1545=EDGE_LOOP('',(#3530,#3531,#3532,#3533));
#1546=EDGE_LOOP('',(#3534,#3535,#3536,#3537));
#1547=EDGE_LOOP('',(#3538,#3539,#3540,#3541));
#1548=EDGE_LOOP('',(#3542,#3543,#3544,#3545));
#1549=EDGE_LOOP('',(#3546,#3547,#3548,#3549,#3550,#3551));
#1550=EDGE_LOOP('',(#3552));
#1551=EDGE_LOOP('',(#3553,#3554,#3555,#3556,#3557,#3558));
#1552=EDGE_LOOP('',(#3559));
#1776=CIRCLE('',#4741,0.7);
#1777=CIRCLE('',#4742,0.7);
#2091=VERTEX_POINT('',#7501);
#2092=VERTEX_POINT('',#7503);
#2093=VERTEX_POINT('',#7507);
#2094=VERTEX_POINT('',#7508);
#2095=VERTEX_POINT('',#7510);
#2096=VERTEX_POINT('',#7512);
#2097=VERTEX_POINT('',#7516);
#2098=VERTEX_POINT('',#7518);
#2099=VERTEX_POINT('',#7522);
#2100=VERTEX_POINT('',#7524);
#2101=VERTEX_POINT('',#7528);
#2102=VERTEX_POINT('',#7530);
#2103=VERTEX_POINT('',#7534);
#2104=VERTEX_POINT('',#7536);
#2569=EDGE_CURVE('',#2091,#2091,#1776,.T.);
#2570=EDGE_CURVE('',#2091,#2092,#595,.T.);
#2571=EDGE_CURVE('',#2092,#2092,#1777,.T.);
#2572=EDGE_CURVE('',#2093,#2094,#596,.T.);
#2573=EDGE_CURVE('',#2094,#2095,#597,.T.);
#2574=EDGE_CURVE('',#2096,#2095,#598,.T.);
#2575=EDGE_CURVE('',#2093,#2096,#599,.T.);
#2576=EDGE_CURVE('',#2097,#2093,#600,.T.);
#2577=EDGE_CURVE('',#2098,#2096,#601,.T.);
#2578=EDGE_CURVE('',#2097,#2098,#602,.T.);
#2579=EDGE_CURVE('',#2099,#2097,#603,.T.);
#2580=EDGE_CURVE('',#2100,#2098,#604,.T.);
#2581=EDGE_CURVE('',#2099,#2100,#605,.T.);
#2582=EDGE_CURVE('',#2101,#2099,#606,.T.);
#2583=EDGE_CURVE('',#2102,#2100,#607,.T.);
#2584=EDGE_CURVE('',#2101,#2102,#608,.T.);
#2585=EDGE_CURVE('',#2103,#2101,#609,.T.);
#2586=EDGE_CURVE('',#2104,#2102,#610,.T.);
#2587=EDGE_CURVE('',#2103,#2104,#611,.T.);
#2588=EDGE_CURVE('',#2094,#2103,#612,.T.);
#2589=EDGE_CURVE('',#2095,#2104,#613,.T.);
#3518=ORIENTED_EDGE('',*,*,#2569,.F.);
#3519=ORIENTED_EDGE('',*,*,#2570,.T.);
#3520=ORIENTED_EDGE('',*,*,#2571,.F.);
#3521=ORIENTED_EDGE('',*,*,#2570,.F.);
#3522=ORIENTED_EDGE('',*,*,#2572,.T.);
#3523=ORIENTED_EDGE('',*,*,#2573,.T.);
#3524=ORIENTED_EDGE('',*,*,#2574,.F.);
#3525=ORIENTED_EDGE('',*,*,#2575,.F.);
#3526=ORIENTED_EDGE('',*,*,#2576,.T.);
#3527=ORIENTED_EDGE('',*,*,#2575,.T.);
#3528=ORIENTED_EDGE('',*,*,#2577,.F.);
#3529=ORIENTED_EDGE('',*,*,#2578,.F.);
#3530=ORIENTED_EDGE('',*,*,#2579,.T.);
#3531=ORIENTED_EDGE('',*,*,#2578,.T.);
#3532=ORIENTED_EDGE('',*,*,#2580,.F.);
#3533=ORIENTED_EDGE('',*,*,#2581,.F.);
#3534=ORIENTED_EDGE('',*,*,#2582,.T.);
#3535=ORIENTED_EDGE('',*,*,#2581,.T.);
#3536=ORIENTED_EDGE('',*,*,#2583,.F.);
#3537=ORIENTED_EDGE('',*,*,#2584,.F.);
#3538=ORIENTED_EDGE('',*,*,#2585,.T.);
#3539=ORIENTED_EDGE('',*,*,#2584,.T.);
#3540=ORIENTED_EDGE('',*,*,#2586,.F.);
#3541=ORIENTED_EDGE('',*,*,#2587,.F.);
#3542=ORIENTED_EDGE('',*,*,#2588,.T.);
#3543=ORIENTED_EDGE('',*,*,#2587,.T.);
#3544=ORIENTED_EDGE('',*,*,#2589,.F.);
#3545=ORIENTED_EDGE('',*,*,#2573,.F.);
#3546=ORIENTED_EDGE('',*,*,#2589,.T.);
#3547=ORIENTED_EDGE('',*,*,#2586,.T.);
#3548=ORIENTED_EDGE('',*,*,#2583,.T.);
#3549=ORIENTED_EDGE('',*,*,#2580,.T.);
#3550=ORIENTED_EDGE('',*,*,#2577,.T.);
#3551=ORIENTED_EDGE('',*,*,#2574,.T.);
#3552=ORIENTED_EDGE('',*,*,#2571,.T.);
#3553=ORIENTED_EDGE('',*,*,#2588,.F.);
#3554=ORIENTED_EDGE('',*,*,#2572,.F.);
#3555=ORIENTED_EDGE('',*,*,#2576,.F.);
#3556=ORIENTED_EDGE('',*,*,#2579,.F.);
#3557=ORIENTED_EDGE('',*,*,#2582,.F.);
#3558=ORIENTED_EDGE('',*,*,#2585,.F.);
#3559=ORIENTED_EDGE('',*,*,#2569,.T.);
#3675=PLANE('',#4743);
#3676=PLANE('',#4744);
#3677=PLANE('',#4745);
#3678=PLANE('',#4746);
#3679=PLANE('',#4747);
#3680=PLANE('',#4748);
#3681=PLANE('',#4749);
#3682=PLANE('',#4750);
#3910=ADVANCED_FACE('',(#1228),#920,.F.);
#3911=ADVANCED_FACE('',(#1229),#3675,.T.);
#3912=ADVANCED_FACE('',(#1230),#3676,.T.);
#3913=ADVANCED_FACE('',(#1231),#3677,.T.);
#3914=ADVANCED_FACE('',(#1232),#3678,.T.);
#3915=ADVANCED_FACE('',(#1233),#3679,.T.);
#3916=ADVANCED_FACE('',(#1234),#3680,.T.);
#3917=ADVANCED_FACE('',(#1235,#999),#3681,.T.);
#3918=ADVANCED_FACE('',(#1236,#1000),#3682,.F.);
#3953=CLOSED_SHELL('',(#3910,#3911,#3912,#3913,#3914,#3915,#3916,#3917,
#3918));
#4739=AXIS2_PLACEMENT_3D('',#7499,#6008,#6009);
#4740=AXIS2_PLACEMENT_3D('',#7500,#6010,#6011);
#4741=AXIS2_PLACEMENT_3D('',#7502,#6012,#6013);
#4742=AXIS2_PLACEMENT_3D('',#7505,#6015,#6016);
#4743=AXIS2_PLACEMENT_3D('',#7506,#6017,#6018);
#4744=AXIS2_PLACEMENT_3D('',#7515,#6023,#6024);
#4745=AXIS2_PLACEMENT_3D('',#7521,#6028,#6029);
#4746=AXIS2_PLACEMENT_3D('',#7527,#6033,#6034);
#4747=AXIS2_PLACEMENT_3D('',#7533,#6038,#6039);
#4748=AXIS2_PLACEMENT_3D('',#7539,#6043,#6044);
#4749=AXIS2_PLACEMENT_3D('',#7542,#6047,#6048);
#4750=AXIS2_PLACEMENT_3D('',#7543,#6049,#6050);
#6008=DIRECTION('axis',(0.,0.,1.));
#6009=DIRECTION('refdir',(1.,0.,0.));
#6010=DIRECTION('center_axis',(0.,0.,1.));
#6011=DIRECTION('ref_axis',(1.,0.,0.));
#6012=DIRECTION('center_axis',(0.,0.,1.));
#6013=DIRECTION('ref_axis',(1.,0.,0.));
#6014=DIRECTION('',(0.,0.,1.));
#6015=DIRECTION('center_axis',(0.,0.,-1.));
#6016=DIRECTION('ref_axis',(1.,0.,0.));
#6017=DIRECTION('center_axis',(-1.60246890531964E-16,-1.,0.));
#6018=DIRECTION('ref_axis',(1.,-1.60246890531964E-16,0.));
#6019=DIRECTION('',(1.,-1.60246890531964E-16,0.));
#6020=DIRECTION('',(0.,0.,1.));
#6021=DIRECTION('',(1.,-1.60246890531964E-16,0.));
#6022=DIRECTION('',(0.,0.,1.));
#6023=DIRECTION('center_axis',(-0.866025403784439,-0.5,0.));
#6024=DIRECTION('ref_axis',(0.5,-0.866025403784439,0.));
#6025=DIRECTION('',(0.5,-0.866025403784439,0.));
#6026=DIRECTION('',(0.5,-0.866025403784439,0.));
#6027=DIRECTION('',(0.,0.,1.));
#6028=DIRECTION('center_axis',(-0.866025403784439,0.5,0.));
#6029=DIRECTION('ref_axis',(-0.5,-0.866025403784439,0.));
#6030=DIRECTION('',(-0.5,-0.866025403784439,0.));
#6031=DIRECTION('',(-0.5,-0.866025403784439,0.));
#6032=DIRECTION('',(0.,0.,1.));
#6033=DIRECTION('center_axis',(1.60246890531964E-16,1.,0.));
#6034=DIRECTION('ref_axis',(-1.,1.60246890531964E-16,0.));
#6035=DIRECTION('',(-1.,1.60246890531964E-16,0.));
#6036=DIRECTION('',(-1.,1.60246890531964E-16,0.));
#6037=DIRECTION('',(0.,0.,1.));
#6038=DIRECTION('center_axis',(0.866025403784439,0.5,0.));
#6039=DIRECTION('ref_axis',(-0.5,0.866025403784439,0.));
#6040=DIRECTION('',(-0.5,0.866025403784439,0.));
#6041=DIRECTION('',(-0.5,0.866025403784439,0.));
#6042=DIRECTION('',(0.,0.,1.));
#6043=DIRECTION('center_axis',(0.866025403784439,-0.5,0.));
#6044=DIRECTION('ref_axis',(0.5,0.866025403784439,0.));
#6045=DIRECTION('',(0.5,0.866025403784439,0.));
#6046=DIRECTION('',(0.5,0.866025403784439,0.));
#6047=DIRECTION('center_axis',(0.,0.,1.));
#6048=DIRECTION('ref_axis',(1.,0.,0.));
#6049=DIRECTION('center_axis',(0.,0.,1.));
#6050=DIRECTION('ref_axis',(1.,0.,0.));
#7499=CARTESIAN_POINT('',(0.,0.,0.));
#7500=CARTESIAN_POINT('Origin',(0.,0.,5.6));
#7501=CARTESIAN_POINT('',(-0.7,-8.57252759403147E-17,5.7));
#7502=CARTESIAN_POINT('Origin',(0.,0.,5.7));
#7503=CARTESIAN_POINT('',(-0.7,8.57252759403147E-17,6.5));
#7504=CARTESIAN_POINT('',(-0.7,-8.57252759403147E-17,5.6));
#7505=CARTESIAN_POINT('Origin',(0.,0.,6.5));
#7506=CARTESIAN_POINT('Origin',(-0.692820323027552,-1.2,5.7));
#7507=CARTESIAN_POINT('',(-0.692820323027552,-1.2,5.7));
#7508=CARTESIAN_POINT('',(0.692820323027551,-1.2,5.7));
#7509=CARTESIAN_POINT('',(-0.692820323027552,-1.2,5.7));
#7510=CARTESIAN_POINT('',(0.692820323027551,-1.2,6.5));
#7511=CARTESIAN_POINT('',(0.692820323027551,-1.2,5.7));
#7512=CARTESIAN_POINT('',(-0.692820323027552,-1.2,6.5));
#7513=CARTESIAN_POINT('',(-0.692820323027552,-1.2,6.5));
#7514=CARTESIAN_POINT('',(-0.692820323027552,-1.2,5.7));
#7515=CARTESIAN_POINT('Origin',(-1.3856406460551,1.69692038195985E-16,5.7));
#7516=CARTESIAN_POINT('',(-1.3856406460551,1.69692038195985E-16,5.7));
#7517=CARTESIAN_POINT('',(-1.3856406460551,1.69692038195985E-16,5.7));
#7518=CARTESIAN_POINT('',(-1.3856406460551,2.22044604925031E-16,6.5));
#7519=CARTESIAN_POINT('',(-1.3856406460551,1.69692038195985E-16,6.5));
#7520=CARTESIAN_POINT('',(-1.3856406460551,1.69692038195985E-16,5.7));
#7521=CARTESIAN_POINT('Origin',(-0.692820323027551,1.2,5.7));
#7522=CARTESIAN_POINT('',(-0.692820323027551,1.2,5.7));
#7523=CARTESIAN_POINT('',(-0.692820323027551,1.2,5.7));
#7524=CARTESIAN_POINT('',(-0.692820323027551,1.2,6.5));
#7525=CARTESIAN_POINT('',(-0.692820323027551,1.2,6.5));
#7526=CARTESIAN_POINT('',(-0.692820323027551,1.2,5.7));
#7527=CARTESIAN_POINT('Origin',(0.692820323027551,1.2,5.7));
#7528=CARTESIAN_POINT('',(0.692820323027551,1.2,5.7));
#7529=CARTESIAN_POINT('',(0.692820323027551,1.2,5.7));
#7530=CARTESIAN_POINT('',(0.692820323027551,1.2,6.5));
#7531=CARTESIAN_POINT('',(0.692820323027551,1.2,6.5));
#7532=CARTESIAN_POINT('',(0.692820323027551,1.2,5.7));
#7533=CARTESIAN_POINT('Origin',(1.3856406460551,0.,5.7));
#7534=CARTESIAN_POINT('',(1.3856406460551,0.,5.7));
#7535=CARTESIAN_POINT('',(1.3856406460551,0.,5.7));
#7536=CARTESIAN_POINT('',(1.3856406460551,0.,6.5));
#7537=CARTESIAN_POINT('',(1.3856406460551,0.,6.5));
#7538=CARTESIAN_POINT('',(1.3856406460551,0.,5.7));
#7539=CARTESIAN_POINT('Origin',(0.692820323027551,-1.2,5.7));
#7540=CARTESIAN_POINT('',(0.692820323027551,-1.2,5.7));
#7541=CARTESIAN_POINT('',(0.692820323027551,-1.2,6.5));
#7542=CARTESIAN_POINT('Origin',(0.,2.22044604925031E-16,6.5));
#7543=CARTESIAN_POINT('Origin',(0.,2.22044604925031E-16,5.7));
#7578=UNCERTAINTY_MEASURE_WITH_UNIT(LENGTH_MEASURE(0.001),#7610,
'DISTANCE_ACCURACY_VALUE',
'Maximum model space distance between geometric entities at asserted c
onnectivities');
#7579=UNCERTAINTY_MEASURE_WITH_UNIT(LENGTH_MEASURE(0.001),#7610,
'DISTANCE_ACCURACY_VALUE',
'Maximum model space distance between geometric entities at asserted c
onnectivities');
#7608=(
GEOMETRIC_REPRESENTATION_CONTEXT(3)
GLOBAL_UNCERTAINTY_ASSIGNED_CONTEXT((#7578))
GLOBAL_UNIT_ASSIGNED_CONTEXT((#7610,#7612,#7613))
REPRESENTATION_CONTEXT('','3D')
);
#7609=(
GEOMETRIC_REPRESENTATION_CONTEXT(3)
GLOBAL_UNCERTAINTY_ASSIGNED_CONTEXT((#7579))
GLOBAL_UNIT_ASSIGNED_CONTEXT((#7610,#7612,#7613))
REPRESENTATION_CONTEXT('','3D')
);
#7610=(
LENGTH_UNIT()
NAMED_UNIT(*)
SI_UNIT(.CENTI.,.METRE.)
);
#7612=(
NAMED_UNIT(*)
PLANE_ANGLE_UNIT()
SI_UNIT($,.RADIAN.)
);
#7613=(
NAMED_UNIT(*)
SI_UNIT($,.STERADIAN.)
SOLID_ANGLE_UNIT()
);
#7642=SHAPE_DEFINITION_REPRESENTATION(#7713,#7748);
#7713=PRODUCT_DEFINITION_SHAPE('',$,#7778);
#7748=SHAPE_REPRESENTATION('',(#4739),#7608);
#7749=PRODUCT_DEFINITION_CONTEXT('part definition',#7838,'design');
#7778=PRODUCT_DEFINITION('M16 hook retaining nut',
'M16 hook retaining nut',#7807,#7749);
#7807=PRODUCT_DEFINITION_FORMATION('',$,#7868);
#7838=APPLICATION_CONTEXT(
'Core Data for Automotive Mechanical Design Process');
#7839=PRODUCT_CONTEXT('part definition',#7838,'mechanical');
#7868=PRODUCT('M16 hook retaining nut','M16 hook retaining nut',
'M16 hook retaining nut',(#7839));
#7932=COLOUR_RGB('Black',0.12,0.14,0.17);
#7933=FILL_AREA_STYLE_COLOUR('',#7932);
#7934=FILL_AREA_STYLE('',(#7933));
#7935=SURFACE_STYLE_FILL_AREA(#7934);
#7936=SURFACE_SIDE_STYLE('',(#7935));
#7937=SURFACE_STYLE_USAGE(.BOTH.,#7936);
#7938=PRESENTATION_STYLE_ASSIGNMENT((#7937));
ENDSEC;
END-ISO-10303-21;
